ISO-10303-21;
HEADER;
FILE_DESCRIPTION (('STEP AP214'),
    '1' );
FILE_NAME ('Part 32,4_Varsayılan.step',
    '2026-10-10T17:45:43',
    ( '' ),
    ( '' ),
    'SwSTEP 2.0',
    'SolidWorks 2024',
    '' );
FILE_SCHEMA (( 'AUTOMOTIVE_DESIGN' ));
ENDSEC;

DATA;
#6=AXIS2_PLACEMENT_3D ( 'NONE', #2010, #2938, #1015 ) ;
#17=DIRECTION ( 'NONE',  ( -0.000000000000000000, -0.000000000000000000, -1.000000000000000000 ) ) ;
#18=DIRECTION ( 'NONE',  ( 0.000000000000000000, 1.000000000000000000, 0.000000000000000000 ) ) ;
#25=FACE_OUTER_BOUND ( 'NONE', #4505, .T. ) ;
#34=EDGE_LOOP ( 'NONE', ( #4986, #287, #6272, #1228, #2299, #5503, #2724 ) ) ;
#48=CARTESIAN_POINT ( 'NONE',  ( 73.99999999999987210, 76.99999716619419132, 276.0000000000000000 ) ) ;
#50=CARTESIAN_POINT ( 'NONE',  ( 64.99991398172927859, 76.99999716619419132, 1.734723475976807094E-15 ) ) ;
#67=LINE ( 'NONE', #4867, #280 ) ;
#69=EDGE_CURVE ( 'NONE', #1244, #5377, #5049, .T. ) ;
#73=FACE_OUTER_BOUND ( 'NONE', #4700, .T. ) ;
#78=DIRECTION ( 'NONE',  ( -0.000000000000000000, -0.000000000000000000, -1.000000000000000000 ) ) ;
#82=ORIENTED_EDGE ( 'NONE', *, *, #1705, .T. ) ;
#89=VECTOR ( 'NONE', #705, 1000.000000000000000 ) ;
#90=CARTESIAN_POINT ( 'NONE',  ( 0.000000000000000000, -25.00000000000000000, 301.0000000000000568 ) ) ;
#99=VECTOR ( 'NONE', #1167, 1000.000000000000000 ) ;
#103=ADVANCED_BREP_SHAPE_REPRESENTATION ( '', ( #4609, #6349 ), #1927 ) ;
#112=CARTESIAN_POINT ( 'NONE',  ( 64.99991398172927859, 32.11307465182860454, 281.0000000000000000 ) ) ;
#122=AXIS2_PLACEMENT_3D ( 'NONE', #5343, #2370, #5378 ) ;
#128=ORIENTED_EDGE ( 'NONE', *, *, #3806, .T. ) ;
#140=CARTESIAN_POINT ( 'NONE',  ( 59.99991398172927859, 0.000000000000000000, 281.0000000000000000 ) ) ;
#149=LINE ( 'NONE', #216, #2805 ) ;
#177=DIRECTION ( 'NONE',  ( -0.000000000000000000, -0.000000000000000000, -1.000000000000000000 ) ) ;
#182=DIRECTION ( 'NONE',  ( 0.000000000000000000, 1.000000000000000000, -1.284980352575412668E-17 ) ) ;
#216=CARTESIAN_POINT ( 'NONE',  ( 0.000000000000000000, 76.99999716619419132, 5.000000000000000000 ) ) ;
#221=VERTEX_POINT ( 'NONE', #5746 ) ;
#225=DIRECTION ( 'NONE',  ( -0.000000000000000000, 0.000000000000000000, 1.000000000000000000 ) ) ;
#231=FACE_OUTER_BOUND ( 'NONE', #5250, .T. ) ;
#235=DIRECTION ( 'NONE',  ( -0.000000000000000000, -1.740526192617802767E-17, 1.000000000000000000 ) ) ;
#241=CARTESIAN_POINT ( 'NONE',  ( 0.000000000000000000, 76.99999716619419132, 5.000000000000000000 ) ) ;
#249=EDGE_CURVE ( 'NONE', #5856, #1997, #4067, .T. ) ;
#258=VERTEX_POINT ( 'NONE', #1877 ) ;
#272=EDGE_CURVE ( 'NONE', #4432, #2238, #5083, .T. ) ;
#280=VECTOR ( 'NONE', #5453, 1000.000000000000000 ) ;
#287=ORIENTED_EDGE ( 'NONE', *, *, #1156, .F. ) ;
#290=CARTESIAN_POINT ( 'NONE',  ( 0.000000000000000000, 0.000000000000000000, 0.000000000000000000 ) ) ;
#296=ORIENTED_EDGE ( 'NONE', *, *, #3074, .T. ) ;
#298=ORIENTED_EDGE ( 'NONE', *, *, #69, .T. ) ;
#317=ORIENTED_EDGE ( 'NONE', *, *, #272, .T. ) ;
#319=ORIENTED_EDGE ( 'NONE', *, *, #4152, .T. ) ;
#332=DIRECTION ( 'NONE',  ( 0.000000000000000000, 1.740526192617802767E-17, -1.000000000000000000 ) ) ;
#334=ORIENTED_EDGE ( 'NONE', *, *, #1705, .F. ) ;
#335=( NAMED_UNIT ( * ) PLANE_ANGLE_UNIT ( ) SI_UNIT ( $, .RADIAN. ) );
#336=VERTEX_POINT ( 'NONE', #3204 ) ;
#338=CARTESIAN_POINT ( 'NONE',  ( 59.99991398172927859, 8.702630963089024930E-17, 276.0000000000000000 ) ) ;
#353=DIRECTION ( 'NONE',  ( -1.000000000000000000, 0.000000000000000000, 0.000000000000000000 ) ) ;
#364=DIRECTION ( 'NONE',  ( -0.000000000000000000, -0.000000000000000000, -1.000000000000000000 ) ) ;
#402=CARTESIAN_POINT ( 'NONE',  ( 0.000000000000000000, -25.00000000000000000, 0.000000000000000000 ) ) ;
#405=EDGE_CURVE ( 'NONE', #6324, #2388, #3760, .T. ) ;
#411=VECTOR ( 'NONE', #4080, 1000.000000000000000 ) ;
#417=CARTESIAN_POINT ( 'NONE',  ( -3.122849337825752983E-15, -17.00000000000000000, 281.0000000000000000 ) ) ;
#421=ORIENTED_EDGE ( 'NONE', *, *, #4564, .T. ) ;
#454=DIRECTION ( 'NONE',  ( -0.000000000000000000, -0.000000000000000000, -1.000000000000000000 ) ) ;
#463=EDGE_CURVE ( 'NONE', #2750, #4432, #4528, .T. ) ;
#488=DIRECTION ( 'NONE',  ( -1.836970198721029194E-16, -1.000000000000000000, 0.000000000000000000 ) ) ;
#490=EDGE_LOOP ( 'NONE', ( #790, #2520, #3675, #298, #2628, #5964 ) ) ;
#529=EDGE_CURVE ( 'NONE', #5958, #3408, #5766, .T. ) ;
#540=CARTESIAN_POINT ( 'NONE',  ( -3.122849337825752983E-15, -17.00000000000000000, 301.0000000000000568 ) ) ;
#541=CYLINDRICAL_SURFACE ( 'NONE', #6, 72.49991987048068154 ) ;
#555=CARTESIAN_POINT ( 'NONE',  ( -3.122849337825752983E-15, -17.00000000000000000, 281.0000000000000000 ) ) ;
#564=CARTESIAN_POINT ( 'NONE',  ( 0.000000000000000000, 0.000000000000000000, -20.00000000000000000 ) ) ;
#568=ORIENTED_EDGE ( 'NONE', *, *, #5155, .T. ) ;
#580=CARTESIAN_POINT ( 'NONE',  ( 0.000000000000000000, 76.99999716619419132, 281.0000000000000000 ) ) ;
#598=PLANE ( 'NONE',  #906 ) ;
#617=FACE_OUTER_BOUND ( 'NONE', #3293, .T. ) ;
#622=DIRECTION ( 'NONE',  ( 0.000000000000000000, -1.000000000000000000, -1.740526192617802767E-17 ) ) ;
#625=PLANE ( 'NONE',  #1215 ) ;
#633=VERTEX_POINT ( 'NONE', #5954 ) ;
#636=DIRECTION ( 'NONE',  ( 0.000000000000000000, -1.000000000000000000, 1.740526192617802767E-17 ) ) ;
#648=DIRECTION ( 'NONE',  ( 1.000000000000000000, 0.000000000000000000, 0.000000000000000000 ) ) ;
#663=DIRECTION ( 'NONE',  ( -0.000000000000000000, -0.000000000000000000, -1.000000000000000000 ) ) ;
#667=DIRECTION ( 'NONE',  ( 0.000000000000000000, -1.740526192617802767E-17, -1.000000000000000000 ) ) ;
#672=LINE ( 'NONE', #5688, #3682 ) ;
#677=CARTESIAN_POINT ( 'NONE',  ( 0.000000000000000000, 0.000000000000000000, 281.0000000000000000 ) ) ;
#693=ADVANCED_FACE ( 'NONE', ( #5493 ), #1074, .T. ) ;
#705=DIRECTION ( 'NONE',  ( -0.000000000000000000, -0.000000000000000000, -1.000000000000000000 ) ) ;
#707=EDGE_CURVE ( 'NONE', #2461, #2595, #1920, .T. ) ;
#710=CARTESIAN_POINT ( 'NONE',  ( 59.99991398172927859, -4.803852291625136032E-15, 5.000000000000004441 ) ) ;
#718=DIRECTION ( 'NONE',  ( -1.836970198721029194E-16, -1.000000000000000000, 0.000000000000000000 ) ) ;
#722=AXIS2_PLACEMENT_3D ( 'NONE', #3398, #4786, #353 ) ;
#745=CIRCLE ( 'NONE', #3199, 25.00000000000000000 ) ;
#771=ORIENTED_EDGE ( 'NONE', *, *, #5541, .T. ) ;
#774=CARTESIAN_POINT ( 'NONE',  ( 59.99991398172927859, 30.92345909152286154, 281.0000000000000000 ) ) ;
#780=ORIENTED_EDGE ( 'NONE', *, *, #1722, .T. ) ;
#790=ORIENTED_EDGE ( 'NONE', *, *, #6358, .T. ) ;
#802=VECTOR ( 'NONE', #718, 1000.000000000000000 ) ;
#827=CARTESIAN_POINT ( 'NONE',  ( 0.000000000000000000, -25.00000000000000000, -20.00000000000000000 ) ) ;
#833=DIRECTION ( 'NONE',  ( 0.000000000000000000, -1.000000000000000000, -1.740526192617802767E-17 ) ) ;
#847=DIRECTION ( 'NONE',  ( -0.000000000000000000, -0.000000000000000000, 1.000000000000000000 ) ) ;
#855=ORIENTED_EDGE ( 'NONE', *, *, #6026, .F. ) ;
#863=ORIENTED_EDGE ( 'NONE', *, *, #1531, .F. ) ;
#871=EDGE_LOOP ( 'NONE', ( #4711, #3275, #3161, #6176 ) ) ;
#891=ORIENTED_EDGE ( 'NONE', *, *, #2377, .F. ) ;
#906=AXIS2_PLACEMENT_3D ( 'NONE', #1949, #2549, #985 ) ;
#921=ORIENTED_EDGE ( 'NONE', *, *, #3930, .F. ) ;
#923=ORIENTED_EDGE ( 'NONE', *, *, #3930, .T. ) ;
#928=DIRECTION ( 'NONE',  ( -0.000000000000000000, -0.000000000000000000, 1.000000000000000000 ) ) ;
#929=ORIENTED_EDGE ( 'NONE', *, *, #2377, .T. ) ;
#931=VECTOR ( 'NONE', #1379, 1000.000000000000000 ) ;
#965=ORIENTED_EDGE ( 'NONE', *, *, #4589, .T. ) ;
#969=LINE ( 'NONE', #2080, #5844 ) ;
#972=CARTESIAN_POINT ( 'NONE',  ( 4.592425496802570422E-15, 25.00000000000000000, 0.000000000000000000 ) ) ;
#985=DIRECTION ( 'NONE',  ( 1.836970198721029194E-16, 1.000000000000000000, 0.000000000000000000 ) ) ;
#1013=CARTESIAN_POINT ( 'NONE',  ( 64.99991398172927859, 76.99999716619419132, 281.0000000000000000 ) ) ;
#1015=DIRECTION ( 'NONE',  ( -1.000000000000000000, 0.000000000000000000, 0.000000000000000000 ) ) ;
#1034=CIRCLE ( 'NONE', #5562, 25.00000000000000000 ) ;
#1035=CARTESIAN_POINT ( 'NONE',  ( -1.239954884136695111E-14, -67.50000000000000000, 276.0000000000000000 ) ) ;
#1041=DIRECTION ( 'NONE',  ( -0.000000000000000000, 1.000000000000000000, -0.000000000000000000 ) ) ;
#1042=LINE ( 'NONE', #112, #2539 ) ;
#1043=FACE_OUTER_BOUND ( 'NONE', #5070, .T. ) ;
#1046=VECTOR ( 'NONE', #1041, 1000.000000000000000 ) ;
#1048=EDGE_CURVE ( 'NONE', #4162, #3651, #2774, .T. ) ;
#1054=LINE ( 'NONE', #5595, #4990 ) ;
#1060=EDGE_CURVE ( 'NONE', #5377, #633, #3845, .T. ) ;
#1068=FACE_OUTER_BOUND ( 'NONE', #871, .T. ) ;
#1073=DIRECTION ( 'NONE',  ( 0.000000000000000000, 1.000000000000000000, 0.000000000000000000 ) ) ;
#1074=PLANE ( 'NONE',  #3046 ) ;
#1087=ORIENTED_EDGE ( 'NONE', *, *, #1531, .T. ) ;
#1089=FACE_OUTER_BOUND ( 'NONE', #2840, .T. ) ;
#1096=ORIENTED_EDGE ( 'NONE', *, *, #1395, .T. ) ;
#1110=ORIENTED_EDGE ( 'NONE', *, *, #5505, .F. ) ;
#1118=EDGE_CURVE ( 'NONE', #6264, #6324, #2972, .T. ) ;
#1126=EDGE_CURVE ( 'NONE', #3949, #3812, #745, .T. ) ;
#1138=FACE_OUTER_BOUND ( 'NONE', #1617, .T. ) ;
#1145=CARTESIAN_POINT ( 'NONE',  ( 0.000000000000000000, -25.00000000000000000, -20.00000000000000000 ) ) ;
#1147=CARTESIAN_POINT ( 'NONE',  ( 0.000000000000000000, 0.000000000000000000, -20.00000000000000000 ) ) ;
#1150=CARTESIAN_POINT ( 'NONE',  ( 0.000000000000000000, 76.99999716619419132, 281.0000000000000000 ) ) ;
#1156=EDGE_CURVE ( 'NONE', #2487, #4674, #2007, .T. ) ;
#1162=ORIENTED_EDGE ( 'NONE', *, *, #3047, .F. ) ;
#1167=DIRECTION ( 'NONE',  ( 0.000000000000000000, 0.000000000000000000, 1.000000000000000000 ) ) ;
#1176=PLANE ( 'NONE',  #1444 ) ;
#1178=APPLICATION_CONTEXT ( 'automotive_design' ) ;
#1211=DIRECTION ( 'NONE',  ( -0.000000000000000000, -0.000000000000000000, -1.000000000000000000 ) ) ;
#1213=( NAMED_UNIT ( * ) SI_UNIT ( $, .STERADIAN. ) SOLID_ANGLE_UNIT ( ) );
#1215=AXIS2_PLACEMENT_3D ( 'NONE', #140, #5423, #5483 ) ;
#1222=PRODUCT ( 'Part 32,4_Varsay\X2\0131\X0\lan', 'Part 32,4_Varsay\X2\0131\X0\lan', '', ( #5630 ) ) ;
#1228=ORIENTED_EDGE ( 'NONE', *, *, #3047, .T. ) ;
#1229=ORIENTED_EDGE ( 'NONE', *, *, #5316, .F. ) ;
#1244=VERTEX_POINT ( 'NONE', #6221 ) ;
#1254=LINE ( 'NONE', #2758, #931 ) ;
#1263=VECTOR ( 'NONE', #4906, 1000.000000000000000 ) ;
#1264=CARTESIAN_POINT ( 'NONE',  ( -1.331801922117356348E-14, -72.49991987048068154, 281.0000000000000000 ) ) ;
#1289=AXIS2_PLACEMENT_3D ( 'NONE', #1147, #5092, #3055 ) ;
#1300=ORIENTED_EDGE ( 'NONE', *, *, #405, .F. ) ;
#1310=SHAPE_REPRESENTATION_RELATIONSHIP ( 'NONE' , 'NONE' ,  #1687, #103 ) ;
#1317=LINE ( 'NONE', #3862, #4507 ) ;
#1327=EDGE_LOOP ( 'NONE', ( #334, #1300, #3470, #1588, #296, #855 ) ) ;
#1374=DIRECTION ( 'NONE',  ( -0.000000000000000000, 0.000000000000000000, -1.000000000000000000 ) ) ;
#1379=DIRECTION ( 'NONE',  ( 0.000000000000000000, 0.000000000000000000, 1.000000000000000000 ) ) ;
#1384=CARTESIAN_POINT ( 'NONE',  ( 3.122849337825750617E-15, -17.00000000000000000, -20.00000000000000000 ) ) ;
#1395=EDGE_CURVE ( 'NONE', #3949, #258, #2475, .T. ) ;
#1418=VECTOR ( 'NONE', #6236, 1000.000000000000000 ) ;
#1421=AXIS2_PLACEMENT_3D ( 'NONE', #2212, #332, #4733 ) ;
#1428=DIRECTION ( 'NONE',  ( 1.836970198721029194E-16, 1.000000000000000000, 0.000000000000000000 ) ) ;
#1435=AXIS2_PLACEMENT_3D ( 'NONE', #5657, #4648, #3104 ) ;
#1444=AXIS2_PLACEMENT_3D ( 'NONE', #677, #225, #648 ) ;
#1457=EDGE_CURVE ( 'NONE', #633, #6022, #1054, .T. ) ;
#1477=ORIENTED_EDGE ( 'NONE', *, *, #529, .T. ) ;
#1484=CARTESIAN_POINT ( 'NONE',  ( 0.000000000000000000, 0.000000000000000000, 301.0000000000000568 ) ) ;
#1489=CARTESIAN_POINT ( 'NONE',  ( 0.000000000000000000, -25.00000000000000000, 301.0000000000000568 ) ) ;
#1495=CYLINDRICAL_SURFACE ( 'NONE', #6144, 17.00000000000000000 ) ;
#1498=ORIENTED_EDGE ( 'NONE', *, *, #3610, .F. ) ;
#1509=DIRECTION ( 'NONE',  ( 0.000000000000000000, 0.000000000000000000, -1.000000000000000000 ) ) ;
#1510=ORIENTED_EDGE ( 'NONE', *, *, #3541, .F. ) ;
#1531=EDGE_CURVE ( 'NONE', #2677, #5616, #3140, .T. ) ;
#1535=VECTOR ( 'NONE', #3068, 1000.000000000000000 ) ;
#1544=CARTESIAN_POINT ( 'NONE',  ( 0.000000000000000000, 0.000000000000000000, 281.0000000000000000 ) ) ;
#1572=CARTESIAN_POINT ( 'NONE',  ( 0.000000000000000000, 0.000000000000000000, -20.00000000000000000 ) ) ;
#1580=ORIENTED_EDGE ( 'NONE', *, *, #4589, .F. ) ;
#1588=ORIENTED_EDGE ( 'NONE', *, *, #2011, .T. ) ;
#1615=LINE ( 'NONE', #1264, #4002 ) ;
#1617=EDGE_LOOP ( 'NONE', ( #5605, #923, #6262, #1580 ) ) ;
#1687=SHAPE_REPRESENTATION ( 'Part 32,4_Varsay\X2\0131\X0\lan', ( #6349 ), #1927 ) ;
#1689=SHAPE_DEFINITION_REPRESENTATION ( #6167, #1687 ) ;
#1701=CARTESIAN_POINT ( 'NONE',  ( 0.000000000000000000, -17.00000000000000000, 5.000000000000004441 ) ) ;
#1705=EDGE_CURVE ( 'NONE', #2388, #3408, #2321, .T. ) ;
#1715=VECTOR ( 'NONE', #4781, 1000.000000000000000 ) ;
#1721=VECTOR ( 'NONE', #4989, 1000.000000000000000 ) ;
#1722=EDGE_CURVE ( 'NONE', #1781, #5856, #149, .T. ) ;
#1732=EDGE_CURVE ( 'NONE', #6264, #2677, #2102, .T. ) ;
#1738=DIRECTION ( 'NONE',  ( 1.000000000000000000, 0.000000000000000000, 0.000000000000000000 ) ) ;
#1746=LINE ( 'NONE', #338, #2185 ) ;
#1781=VERTEX_POINT ( 'NONE', #241 ) ;
#1793=CYLINDRICAL_SURFACE ( 'NONE', #722, 25.00000000000000000 ) ;
#1824=ORIENTED_EDGE ( 'NONE', *, *, #6358, .F. ) ;
#1825=ORIENTED_EDGE ( 'NONE', *, *, #3218, .T. ) ;
#1834=EDGE_CURVE ( 'NONE', #5091, #633, #4846, .T. ) ;
#1860=ORIENTED_EDGE ( 'NONE', *, *, #1060, .F. ) ;
#1877=CARTESIAN_POINT ( 'NONE',  ( 25.00000000000000000, 0.000000000000000000, 0.000000000000000000 ) ) ;
#1883=ORIENTED_EDGE ( 'NONE', *, *, #6026, .T. ) ;
#1885=ADVANCED_FACE ( 'NONE', ( #3452 ), #2392, .F. ) ;
#1887=LINE ( 'NONE', #827, #1418 ) ;
#1917=ORIENTED_EDGE ( 'NONE', *, *, #4670, .F. ) ;
#1920=CIRCLE ( 'NONE', #6040, 72.49991987048069575 ) ;
#1927=( GEOMETRIC_REPRESENTATION_CONTEXT ( 3 ) GLOBAL_UNCERTAINTY_ASSIGNED_CONTEXT ( ( #2692 ) ) GLOBAL_UNIT_ASSIGNED_CONTEXT ( ( #5255, #3769, #1213 ) ) REPRESENTATION_CONTEXT ( 'NONE', 'WORKASPACE' ) );
#1941=CARTESIAN_POINT ( 'NONE',  ( -0.000000000000000000, 76.99999716619419132, 0.000000000000000000 ) ) ;
#1949=CARTESIAN_POINT ( 'NONE',  ( -3.081487911019577365E-30, 5.660601460262082306E-46, 281.0000000000000000 ) ) ;
#1966=CARTESIAN_POINT ( 'NONE',  ( 0.000000000000000000, 25.00000000000000000, -20.00000000000000000 ) ) ;
#1980=CARTESIAN_POINT ( 'NONE',  ( 0.000000000000000000, 76.99999716619419132, 281.0000000000000000 ) ) ;
#1993=DIRECTION ( 'NONE',  ( -0.000000000000000000, -0.000000000000000000, 1.000000000000000000 ) ) ;
#1997=VERTEX_POINT ( 'NONE', #1701 ) ;
#2007=LINE ( 'NONE', #5916, #5573 ) ;
#2008=PRODUCT_DEFINITION ( 'UNKNOWN', '', #4145, #5528 ) ;
#2010=CARTESIAN_POINT ( 'NONE',  ( 0.000000000000000000, 0.000000000000000000, 281.0000000000000000 ) ) ;
#2011=EDGE_CURVE ( 'NONE', #6264, #336, #1746, .T. ) ;
#2020=ORIENTED_EDGE ( 'NONE', *, *, #4201, .T. ) ;
#2030=CARTESIAN_POINT ( 'NONE',  ( 0.000000000000000000, 17.00000000000000000, 276.0000000000000000 ) ) ;
#2044=ORIENTED_EDGE ( 'NONE', *, *, #1118, .T. ) ;
#2053=AXIS2_PLACEMENT_3D ( 'NONE', #3009, #2457, #18 ) ;
#2057=ORIENTED_EDGE ( 'NONE', *, *, #4660, .T. ) ;
#2071=EDGE_LOOP ( 'NONE', ( #5252, #891, #5516, #128 ) ) ;
#2080=CARTESIAN_POINT ( 'NONE',  ( -3.081487911019577365E-30, 5.660601460262082306E-46, 281.0000000000000000 ) ) ;
#2091=CARTESIAN_POINT ( 'NONE',  ( 0.000000000000000000, 76.99999716619419132, 276.0000000000000000 ) ) ;
#2102=LINE ( 'NONE', #4547, #4454 ) ;
#2111=ADVANCED_FACE ( 'NONE', ( #3412 ), #4376, .T. ) ;
#2114=ORIENTED_EDGE ( 'NONE', *, *, #69, .F. ) ;
#2120=CYLINDRICAL_SURFACE ( 'NONE', #3370, 25.00000000000000000 ) ;
#2134=CARTESIAN_POINT ( 'NONE',  ( 3.122849337825746672E-15, 17.00000000000000000, 281.0000000000000000 ) ) ;
#2150=DIRECTION ( 'NONE',  ( -1.836970198721029194E-16, -1.000000000000000000, 0.000000000000000000 ) ) ;
#2158=AXIS2_PLACEMENT_3D ( 'NONE', #6021, #6114, #5571 ) ;
#2168=CYLINDRICAL_SURFACE ( 'NONE', #1435, 67.50000000000000000 ) ;
#2182=FACE_OUTER_BOUND ( 'NONE', #34, .T. ) ;
#2185=VECTOR ( 'NONE', #3254, 1000.000000000000000 ) ;
#2196=CARTESIAN_POINT ( 'NONE',  ( 0.000000000000000000, 0.000000000000000000, -20.00000000000000000 ) ) ;
#2212=CARTESIAN_POINT ( 'NONE',  ( 73.99999999999987210, 76.99999716619419132, 276.0000000000000000 ) ) ;
#2238=VERTEX_POINT ( 'NONE', #5877 ) ;
#2239=CIRCLE ( 'NONE', #5859, 25.00000000000000000 ) ;
#2240=CARTESIAN_POINT ( 'NONE',  ( 64.99991398172927859, 32.11307465182860454, 1.734723475976807094E-15 ) ) ;
#2242=DIRECTION ( 'NONE',  ( 0.000000000000000000, 0.000000000000000000, 1.000000000000000000 ) ) ;
#2244=VECTOR ( 'NONE', #454, 1000.000000000000000 ) ;
#2261=AXIS2_PLACEMENT_3D ( 'NONE', #3122, #235, #5165 ) ;
#2285=ORIENTED_EDGE ( 'NONE', *, *, #463, .F. ) ;
#2299=ORIENTED_EDGE ( 'NONE', *, *, #707, .T. ) ;
#2301=VERTEX_POINT ( 'NONE', #3026 ) ;
#2321=CIRCLE ( 'NONE', #5934, 17.00000000000000000 ) ;
#2341=ORIENTED_EDGE ( 'NONE', *, *, #1126, .F. ) ;
#2370=DIRECTION ( 'NONE',  ( -0.000000000000000000, -0.000000000000000000, -1.000000000000000000 ) ) ;
#2377=EDGE_CURVE ( 'NONE', #3651, #3949, #2523, .T. ) ;
#2386=DIRECTION ( 'NONE',  ( 0.000000000000000000, 0.000000000000000000, -1.000000000000000000 ) ) ;
#2388=VERTEX_POINT ( 'NONE', #2030 ) ;
#2391=ORIENTED_EDGE ( 'NONE', *, *, #405, .T. ) ;
#2392=PLANE ( 'NONE',  #5588 ) ;
#2419=DIRECTION ( 'NONE',  ( -1.836970198721029194E-16, -1.000000000000000000, 0.000000000000000000 ) ) ;
#2425=CARTESIAN_POINT ( 'NONE',  ( 0.000000000000000000, 0.000000000000000000, 281.0000000000000000 ) ) ;
#2451=AXIS2_PLACEMENT_3D ( 'NONE', #3448, #4421, #2969 ) ;
#2457=DIRECTION ( 'NONE',  ( 0.000000000000000000, 1.740526192617802767E-17, -1.000000000000000000 ) ) ;
#2461=VERTEX_POINT ( 'NONE', #2240 ) ;
#2467=ADVANCED_FACE ( 'NONE', ( #5600 ), #3701, .F. ) ;
#2475=LINE ( 'NONE', #3473, #2587 ) ;
#2487=VERTEX_POINT ( 'NONE', #4731 ) ;
#2501=DIRECTION ( 'NONE',  ( 1.000000000000000000, -1.836970198721029194E-16, 0.000000000000000000 ) ) ;
#2513=CARTESIAN_POINT ( 'NONE',  ( 0.000000000000000000, 17.00000000000000000, 5.000000000000004441 ) ) ;
#2520=ORIENTED_EDGE ( 'NONE', *, *, #4682, .T. ) ;
#2523=CIRCLE ( 'NONE', #1289, 25.00000000000000000 ) ;
#2539=VECTOR ( 'NONE', #78, 1000.000000000000000 ) ;
#2549=DIRECTION ( 'NONE',  ( 1.000000000000000000, -1.836970198721029194E-16, 0.000000000000000000 ) ) ;
#2551=VECTOR ( 'NONE', #6320, 1000.000000000000000 ) ;
#2553=ORIENTED_EDGE ( 'NONE', *, *, #1156, .T. ) ;
#2561=ORIENTED_EDGE ( 'NONE', *, *, #5104, .F. ) ;
#2562=AXIS2_PLACEMENT_3D ( 'NONE', #4953, #2501, #4461 ) ;
#2566=DIRECTION ( 'NONE',  ( -0.000000000000000000, -0.000000000000000000, 1.000000000000000000 ) ) ;
#2575=VECTOR ( 'NONE', #833, 1000.000000000000000 ) ;
#2583=ORIENTED_EDGE ( 'NONE', *, *, #529, .F. ) ;
#2587=VECTOR ( 'NONE', #1993, 1000.000000000000000 ) ;
#2595=VERTEX_POINT ( 'NONE', #5801 ) ;
#2600=ORIENTED_EDGE ( 'NONE', *, *, #1457, .F. ) ;
#2617=CARTESIAN_POINT ( 'NONE',  ( 0.000000000000000000, 25.00000000000000000, 281.0000000000000000 ) ) ;
#2619=CARTESIAN_POINT ( 'NONE',  ( 3.122849337825746672E-15, 17.00000000000000000, -20.00000000000000000 ) ) ;
#2627=FACE_OUTER_BOUND ( 'NONE', #2071, .T. ) ;
#2628=ORIENTED_EDGE ( 'NONE', *, *, #1060, .T. ) ;
#2655=DIRECTION ( 'NONE',  ( 0.000000000000000000, -1.000000000000000000, 1.740526192617802767E-17 ) ) ;
#2669=ORIENTED_EDGE ( 'NONE', *, *, #5541, .F. ) ;
#2677=VERTEX_POINT ( 'NONE', #6170 ) ;
#2688=ORIENTED_EDGE ( 'NONE', *, *, #1126, .T. ) ;
#2692=UNCERTAINTY_MEASURE_WITH_UNIT (LENGTH_MEASURE( 1.000000000000000082E-05 ), #5255, 'distance_accuracy_value', 'NONE');
#2724=ORIENTED_EDGE ( 'NONE', *, *, #5756, .F. ) ;
#2735=ORIENTED_EDGE ( 'NONE', *, *, #1457, .T. ) ;
#2750=VERTEX_POINT ( 'NONE', #4681 ) ;
#2758=CARTESIAN_POINT ( 'NONE',  ( 3.122849337825746672E-15, 17.00000000000000000, 281.0000000000000000 ) ) ;
#2774=LINE ( 'NONE', #3784, #5110 ) ;
#2792=LINE ( 'NONE', #5770, #3712 ) ;
#2800=DIRECTION ( 'NONE',  ( -1.000000000000000000, 0.000000000000000000, 0.000000000000000000 ) ) ;
#2805=VECTOR ( 'NONE', #636, 1000.000000000000000 ) ;
#2840=EDGE_LOOP ( 'NONE', ( #780, #3751, #5763, #2561, #863, #3801 ) ) ;
#2841=ORIENTED_EDGE ( 'NONE', *, *, #4098, .T. ) ;
#2852=CARTESIAN_POINT ( 'NONE',  ( 0.000000000000000000, 76.99999716619419132, 281.0000000000000000 ) ) ;
#2863=ORIENTED_EDGE ( 'NONE', *, *, #3610, .T. ) ;
#2878=ORIENTED_EDGE ( 'NONE', *, *, #1048, .F. ) ;
#2890=CARTESIAN_POINT ( 'NONE',  ( 59.99991398172927859, 76.99999716619419132, 276.0000000000000000 ) ) ;
#2935=DIRECTION ( 'NONE',  ( -1.000000000000000000, 0.000000000000000000, 0.000000000000000000 ) ) ;
#2938=DIRECTION ( 'NONE',  ( -0.000000000000000000, -0.000000000000000000, -1.000000000000000000 ) ) ;
#2969=DIRECTION ( 'NONE',  ( 0.000000000000000000, 1.000000000000000000, -1.740526192617802767E-17 ) ) ;
#2972=LINE ( 'NONE', #48, #5678 ) ;
#2985=AXIS2_PLACEMENT_3D ( 'NONE', #4139, #3184, #1738 ) ;
#3009=CARTESIAN_POINT ( 'NONE',  ( 0.000000000000000000, 0.000000000000000000, 276.0000000000000000 ) ) ;
#3014=PLANE ( 'NONE',  #2562 ) ;
#3019=DIRECTION ( 'NONE',  ( -0.000000000000000000, -0.000000000000000000, -1.000000000000000000 ) ) ;
#3021=ORIENTED_EDGE ( 'NONE', *, *, #5341, .T. ) ;
#3026=CARTESIAN_POINT ( 'NONE',  ( 0.000000000000000000, -67.50000000000001421, 5.000000000000002665 ) ) ;
#3035=LINE ( 'NONE', #50, #1535 ) ;
#3039=EDGE_LOOP ( 'NONE', ( #2583, #2057, #1510, #82 ) ) ;
#3046=AXIS2_PLACEMENT_3D ( 'NONE', #2196, #4154, #3265 ) ;
#3047=EDGE_CURVE ( 'NONE', #6022, #2461, #3035, .T. ) ;
#3050=CIRCLE ( 'NONE', #5640, 25.00000000000000000 ) ;
#3051=ADVANCED_FACE ( 'NONE', ( #1043 ), #541, .T. ) ;
#3055=DIRECTION ( 'NONE',  ( -1.000000000000000000, 0.000000000000000000, 0.000000000000000000 ) ) ;
#3068=DIRECTION ( 'NONE',  ( 0.000000000000000000, -1.000000000000000000, 0.000000000000000000 ) ) ;
#3071=ORIENTED_EDGE ( 'NONE', *, *, #5756, .T. ) ;
#3074=EDGE_CURVE ( 'NONE', #336, #5800, #5772, .T. ) ;
#3091=DIRECTION ( 'NONE',  ( -0.000000000000000000, -0.000000000000000000, 1.000000000000000000 ) ) ;
#3104=DIRECTION ( 'NONE',  ( -1.000000000000000000, 0.000000000000000000, 0.000000000000000000 ) ) ;
#3113=DIRECTION ( 'NONE',  ( 0.000000000000000000, 0.000000000000000000, -1.000000000000000000 ) ) ;
#3116=DIRECTION ( 'NONE',  ( 0.000000000000000000, 0.000000000000000000, -1.000000000000000000 ) ) ;
#3117=DIRECTION ( 'NONE',  ( 0.000000000000000000, 1.000000000000000000, 0.000000000000000000 ) ) ;
#3122=CARTESIAN_POINT ( 'NONE',  ( 0.000000000000000000, -4.890878601256026467E-15, 281.0000000000000000 ) ) ;
#3135=LINE ( 'NONE', #5112, #89 ) ;
#3140=LINE ( 'NONE', #710, #6239 ) ;
#3160=EDGE_LOOP ( 'NONE', ( #5273, #2735, #4458, #421, #3990, #6313, #2044, #1498 ) ) ;
#3161=ORIENTED_EDGE ( 'NONE', *, *, #4098, .F. ) ;
#3175=CIRCLE ( 'NONE', #6166, 67.50000000000000000 ) ;
#3180=CARTESIAN_POINT ( 'NONE',  ( 0.000000000000000000, 0.000000000000000000, 5.000000000000004441 ) ) ;
#3184=DIRECTION ( 'NONE',  ( -0.000000000000000000, 0.000000000000000000, 1.000000000000000000 ) ) ;
#3199=AXIS2_PLACEMENT_3D ( 'NONE', #564, #3116, #2935 ) ;
#3204=CARTESIAN_POINT ( 'NONE',  ( 59.99991398172927859, 30.92345909152286154, 276.0000000000000000 ) ) ;
#3218=EDGE_CURVE ( 'NONE', #1244, #2595, #1615, .T. ) ;
#3254=DIRECTION ( 'NONE',  ( 0.000000000000000000, -1.000000000000000000, -1.740526192617802767E-17 ) ) ;
#3265=DIRECTION ( 'NONE',  ( -1.000000000000000000, 0.000000000000000000, -0.000000000000000000 ) ) ;
#3266=CARTESIAN_POINT ( 'NONE',  ( 64.99991398172927859, 32.11307465182860454, 281.0000000000000000 ) ) ;
#3275=ORIENTED_EDGE ( 'NONE', *, *, #5155, .F. ) ;
#3276=DIRECTION ( 'NONE',  ( -0.000000000000000000, -0.000000000000000000, -1.000000000000000000 ) ) ;
#3293=EDGE_LOOP ( 'NONE', ( #2600, #1860, #6053, #1162 ) ) ;
#3303=DIRECTION ( 'NONE',  ( -0.000000000000000000, -0.000000000000000000, -1.000000000000000000 ) ) ;
#3318=ORIENTED_EDGE ( 'NONE', *, *, #5945, .F. ) ;
#3364=VECTOR ( 'NONE', #4997, 1000.000000000000000 ) ;
#3370=AXIS2_PLACEMENT_3D ( 'NONE', #1572, #3091, #4077 ) ;
#3398=CARTESIAN_POINT ( 'NONE',  ( 0.000000000000000000, 0.000000000000000000, 301.0000000000000568 ) ) ;
#3408=VERTEX_POINT ( 'NONE', #4504 ) ;
#3412=FACE_OUTER_BOUND ( 'NONE', #4576, .T. ) ;
#3437=ADVANCED_FACE ( 'NONE', ( #2182 ), #5577, .F. ) ;
#3448=CARTESIAN_POINT ( 'NONE',  ( 73.99999999999987210, 76.99999716619419132, 5.000000000000000000 ) ) ;
#3452=FACE_OUTER_BOUND ( 'NONE', #4373, .T. ) ;
#3456=DIRECTION ( 'NONE',  ( -1.000000000000000000, 0.000000000000000000, 0.000000000000000000 ) ) ;
#3470=ORIENTED_EDGE ( 'NONE', *, *, #1118, .F. ) ;
#3473=CARTESIAN_POINT ( 'NONE',  ( 25.00000000000000000, 0.000000000000000000, -20.00000000000000000 ) ) ;
#3541=EDGE_CURVE ( 'NONE', #2388, #221, #1254, .T. ) ;
#3542=LINE ( 'NONE', #5639, #802 ) ;
#3549=CARTESIAN_POINT ( 'NONE',  ( 59.99991398172927859, 30.92345909152286154, 5.000000000000004441 ) ) ;
#3566=CARTESIAN_POINT ( 'NONE',  ( 0.000000000000000000, 0.000000000000000000, 0.000000000000000000 ) ) ;
#3567=ORIENTED_EDGE ( 'NONE', *, *, #1722, .F. ) ;
#3610=EDGE_CURVE ( 'NONE', #5091, #6324, #3931, .T. ) ;
#3615=ORIENTED_EDGE ( 'NONE', *, *, #4660, .F. ) ;
#3648=CARTESIAN_POINT ( 'NONE',  ( 0.000000000000000000, 0.000000000000000000, 5.000000000000004441 ) ) ;
#3651=VERTEX_POINT ( 'NONE', #1966 ) ;
#3664=DIRECTION ( 'NONE',  ( -1.000000000000000000, -0.000000000000000000, -0.000000000000000000 ) ) ;
#3675=ORIENTED_EDGE ( 'NONE', *, *, #5945, .T. ) ;
#3682=VECTOR ( 'NONE', #2419, 1000.000000000000000 ) ;
#3697=CARTESIAN_POINT ( 'NONE',  ( 25.00000000000000000, 0.000000000000000000, -20.00000000000000000 ) ) ;
#3701=CYLINDRICAL_SURFACE ( 'NONE', #4379, 17.00000000000000000 ) ;
#3712=VECTOR ( 'NONE', #5733, 1000.000000000000000 ) ;
#3725=ORIENTED_EDGE ( 'NONE', *, *, #272, .F. ) ;
#3736=EDGE_CURVE ( 'NONE', #3651, #4674, #5598, .T. ) ;
#3751=ORIENTED_EDGE ( 'NONE', *, *, #249, .T. ) ;
#3760=LINE ( 'NONE', #5726, #2575 ) ;
#3769=( NAMED_UNIT ( * ) PLANE_ANGLE_UNIT ( ) SI_UNIT ( $, .RADIAN. ) );
#3784=CARTESIAN_POINT ( 'NONE',  ( 0.000000000000000000, 25.00000000000000000, -20.00000000000000000 ) ) ;
#3801=ORIENTED_EDGE ( 'NONE', *, *, #5817, .T. ) ;
#3802=CARTESIAN_POINT ( 'NONE',  ( 0.000000000000000000, 25.00000000000000000, 301.0000000000000568 ) ) ;
#3806=EDGE_CURVE ( 'NONE', #4674, #258, #1034, .T. ) ;
#3810=ADVANCED_FACE ( 'NONE', ( #4594 ), #1176, .T. ) ;
#3812=VERTEX_POINT ( 'NONE', #1145 ) ;
#3819=EDGE_LOOP ( 'NONE', ( #3318, #3725, #771, #1477, #1883, #965, #1229, #4745, #4719, #3021, #2020, #5704 ) ) ;
#3845=LINE ( 'NONE', #1013, #1046 ) ;
#3862=CARTESIAN_POINT ( 'NONE',  ( -1.239954884136695111E-14, -67.50000000000000000, 281.0000000000000000 ) ) ;
#3884=ADVANCED_FACE ( 'NONE', ( #2627 ), #5633, .T. ) ;
#3916=ADVANCED_FACE ( 'NONE', ( #617 ), #4529, .T. ) ;
#3930=EDGE_CURVE ( 'NONE', #336, #5616, #4237, .T. ) ;
#3931=LINE ( 'NONE', #580, #5463 ) ;
#3949=VERTEX_POINT ( 'NONE', #3697 ) ;
#3951=ORIENTED_EDGE ( 'NONE', *, *, #4000, .T. ) ;
#3990=ORIENTED_EDGE ( 'NONE', *, *, #5817, .F. ) ;
#4000=EDGE_CURVE ( 'NONE', #3812, #5753, #2792, .T. ) ;
#4002=VECTOR ( 'NONE', #177, 1000.000000000000000 ) ;
#4007=ORIENTED_EDGE ( 'NONE', *, *, #1732, .T. ) ;
#4015=CARTESIAN_POINT ( 'NONE',  ( 0.000000000000000000, 25.00000000000000000, -20.00000000000000000 ) ) ;
#4020=CARTESIAN_POINT ( 'NONE',  ( 64.99991398172927859, 76.99999716619419132, 1.734723475976807094E-15 ) ) ;
#4026=LINE ( 'NONE', #540, #3364 ) ;
#4040=ORIENTED_EDGE ( 'NONE', *, *, #4152, .F. ) ;
#4041=MECHANICAL_DESIGN_GEOMETRIC_PRESENTATION_REPRESENTATION('',(#5447),#5133);
#4053=ORIENTED_EDGE ( 'NONE', *, *, #463, .T. ) ;
#4067=CIRCLE ( 'NONE', #5217, 17.00000000000000000 ) ;
#4077=DIRECTION ( 'NONE',  ( 1.000000000000000000, 0.000000000000000000, 0.000000000000000000 ) ) ;
#4080=DIRECTION ( 'NONE',  ( 0.000000000000000000, 0.000000000000000000, 1.000000000000000000 ) ) ;
#4086=CIRCLE ( 'NONE', #5348, 17.00000000000000000 ) ;
#4089=CARTESIAN_POINT ( 'NONE',  ( 0.000000000000000000, 0.000000000000000000, 276.0000000000000000 ) ) ;
#4098=EDGE_CURVE ( 'NONE', #5753, #4162, #5754, .T. ) ;
#4138=CARTESIAN_POINT ( 'NONE',  ( 3.122849337825750617E-15, -17.00000000000000000, 301.0000000000000568 ) ) ;
#4139=CARTESIAN_POINT ( 'NONE',  ( 0.000000000000000000, 0.000000000000000000, 0.000000000000000000 ) ) ;
#4145=PRODUCT_DEFINITION_FORMATION_WITH_SPECIFIED_SOURCE ( 'ANY', '', #1222, .NOT_KNOWN. ) ;
#4152=EDGE_CURVE ( 'NONE', #2750, #5198, #3135, .T. ) ;
#4154=DIRECTION ( 'NONE',  ( 0.000000000000000000, 0.000000000000000000, -1.000000000000000000 ) ) ;
#4162=VERTEX_POINT ( 'NONE', #2619 ) ;
#4169=DIRECTION ( 'NONE',  ( 1.000000000000000000, 0.000000000000000000, 0.000000000000000000 ) ) ;
#4171=PLANE ( 'NONE',  #1421 ) ;
#4201=EDGE_CURVE ( 'NONE', #5742, #2595, #672, .T. ) ;
#4210=DIRECTION ( 'NONE',  ( -1.000000000000000000, 0.000000000000000000, 0.000000000000000000 ) ) ;
#4219=EDGE_LOOP ( 'NONE', ( #929, #2688, #3951, #2841, #6084 ) ) ;
#4237=LINE ( 'NONE', #774, #6079 ) ;
#4239=CARTESIAN_POINT ( 'NONE',  ( 0.000000000000000000, 0.000000000000000000, 281.0000000000000000 ) ) ;
#4245=CARTESIAN_POINT ( 'NONE',  ( 0.000000000000000000, 0.000000000000000000, 301.0000000000000568 ) ) ;
#4294=ORIENTED_EDGE ( 'NONE', *, *, #707, .F. ) ;
#4321=AXIS2_PLACEMENT_3D ( 'NONE', #5214, #5185, #1374 ) ;
#4323=CLOSED_SHELL ( 'NONE', ( #5937, #3810, #3437, #5436, #4965, #5245, #3051, #3916, #4473, #1885, #5938, #4469, #6089, #2467, #5443, #3884, #693, #4823, #2111 ) ) ;
#4341=LINE ( 'NONE', #3802, #2551 ) ;
#4346=DIRECTION ( 'NONE',  ( -1.000000000000000000, 0.000000000000000000, 0.000000000000000000 ) ) ;
#4351=APPLICATION_CONTEXT ( 'automotive_design' ) ;
#4373=EDGE_LOOP ( 'NONE', ( #2391, #4485, #4664, #319, #1824, #2863 ) ) ;
#4376=PLANE ( 'NONE',  #5102 ) ;
#4379=AXIS2_PLACEMENT_3D ( 'NONE', #4239, #1211, #4210 ) ;
#4385=CARTESIAN_POINT ( 'NONE',  ( -3.081487911019577365E-30, 5.660601460262082306E-46, 281.0000000000000000 ) ) ;
#4404=AXIS2_PLACEMENT_3D ( 'NONE', #5957, #928, #5407 ) ;
#4421=DIRECTION ( 'NONE',  ( 0.000000000000000000, -1.740526192617802767E-17, -1.000000000000000000 ) ) ;
#4432=VERTEX_POINT ( 'NONE', #1489 ) ;
#4454=VECTOR ( 'NONE', #663, 1000.000000000000000 ) ;
#4458=ORIENTED_EDGE ( 'NONE', *, *, #5839, .F. ) ;
#4461=DIRECTION ( 'NONE',  ( 1.836970198721029194E-16, 1.000000000000000000, 0.000000000000000000 ) ) ;
#4464=DIRECTION ( 'NONE',  ( -0.000000000000000000, -0.000000000000000000, -1.000000000000000000 ) ) ;
#4469=ADVANCED_FACE ( 'NONE', ( #1089 ), #5944, .F. ) ;
#4473=ADVANCED_FACE ( 'NONE', ( #73 ), #625, .T. ) ;
#4485=ORIENTED_EDGE ( 'NONE', *, *, #3541, .T. ) ;
#4504=CARTESIAN_POINT ( 'NONE',  ( 0.000000000000000000, -17.00000000000000000, 276.0000000000000000 ) ) ;
#4505=EDGE_LOOP ( 'NONE', ( #2553, #4675, #2878, #568, #3567, #5708 ) ) ;
#4507=VECTOR ( 'NONE', #364, 1000.000000000000000 ) ;
#4528=CIRCLE ( 'NONE', #122, 25.00000000000000000 ) ;
#4529=PLANE ( 'NONE',  #4321 ) ;
#4532=PLANE ( 'NONE',  #5520 ) ;
#4547=CARTESIAN_POINT ( 'NONE',  ( 59.99991398172927859, 76.99999716619419132, 281.0000000000000000 ) ) ;
#4564=EDGE_CURVE ( 'NONE', #2487, #1781, #4702, .T. ) ;
#4576=EDGE_LOOP ( 'NONE', ( #2285, #1917, #3615, #2669 ) ) ;
#4589=EDGE_CURVE ( 'NONE', #5800, #2301, #1317, .T. ) ;
#4594=FACE_OUTER_BOUND ( 'NONE', #490, .T. ) ;
#4604=CARTESIAN_POINT ( 'NONE',  ( 0.000000000000000000, 76.99999716619419132, 0.000000000000000000 ) ) ;
#4609=MANIFOLD_SOLID_BREP ( 'Mirror2', #4323 ) ;
#4648=DIRECTION ( 'NONE',  ( -0.000000000000000000, -0.000000000000000000, -1.000000000000000000 ) ) ;
#4660=EDGE_CURVE ( 'NONE', #5958, #221, #4086, .T. ) ;
#4664=ORIENTED_EDGE ( 'NONE', *, *, #4670, .T. ) ;
#4670=EDGE_CURVE ( 'NONE', #221, #2750, #4341, .T. ) ;
#4674=VERTEX_POINT ( 'NONE', #972 ) ;
#4675=ORIENTED_EDGE ( 'NONE', *, *, #3736, .F. ) ;
#4681=CARTESIAN_POINT ( 'NONE',  ( 0.000000000000000000, 25.00000000000000000, 301.0000000000000568 ) ) ;
#4682=EDGE_CURVE ( 'NONE', #5198, #2238, #2239, .T. ) ;
#4700=EDGE_LOOP ( 'NONE', ( #5152, #4007, #1087, #921 ) ) ;
#4702=LINE ( 'NONE', #4604, #411 ) ;
#4711=ORIENTED_EDGE ( 'NONE', *, *, #249, .F. ) ;
#4713=DIRECTION ( 'NONE',  ( 1.000000000000000000, 0.000000000000000000, 0.000000000000000000 ) ) ;
#4719=ORIENTED_EDGE ( 'NONE', *, *, #4000, .F. ) ;
#4731=CARTESIAN_POINT ( 'NONE',  ( 0.000000000000000000, 76.99999716619419132, 0.000000000000000000 ) ) ;
#4733=DIRECTION ( 'NONE',  ( 0.000000000000000000, 1.000000000000000000, 1.740526192617802767E-17 ) ) ;
#4737=( NAMED_UNIT ( * ) SI_UNIT ( $, .STERADIAN. ) SOLID_ANGLE_UNIT ( ) );
#4745=ORIENTED_EDGE ( 'NONE', *, *, #4768, .T. ) ;
#4761=FACE_OUTER_BOUND ( 'NONE', #5081, .T. ) ;
#4768=EDGE_CURVE ( 'NONE', #1997, #5753, #4897, .T. ) ;
#4781=DIRECTION ( 'NONE',  ( 0.000000000000000000, -1.000000000000000000, 1.740526192617802767E-17 ) ) ;
#4786=DIRECTION ( 'NONE',  ( -0.000000000000000000, -0.000000000000000000, -1.000000000000000000 ) ) ;
#4812=FACE_OUTER_BOUND ( 'NONE', #3819, .T. ) ;
#4823=ADVANCED_FACE ( 'NONE', ( #4761 ), #1793, .T. ) ;
#4839=CARTESIAN_POINT ( 'NONE',  ( 0.000000000000000000, 0.000000000000000000, 0.000000000000000000 ) ) ;
#4846=LINE ( 'NONE', #1980, #1263 ) ;
#4863=( LENGTH_UNIT ( ) NAMED_UNIT ( * ) SI_UNIT ( .MILLI., .METRE. ) );
#4867=CARTESIAN_POINT ( 'NONE',  ( 73.99999999999987210, 76.99999716619419132, 5.000000000000000000 ) ) ;
#4897=LINE ( 'NONE', #555, #2244 ) ;
#4898=DIRECTION ( 'NONE',  ( -1.000000000000000000, 0.000000000000000000, 0.000000000000000000 ) ) ;
#4906=DIRECTION ( 'NONE',  ( 1.000000000000000000, 0.000000000000000000, 0.000000000000000000 ) ) ;
#4933=LINE ( 'NONE', #1941, #1721 ) ;
#4953=CARTESIAN_POINT ( 'NONE',  ( -3.081487911019577365E-30, 5.660601460262082306E-46, 281.0000000000000000 ) ) ;
#4965=ADVANCED_FACE ( 'NONE', ( #25 ), #3014, .F. ) ;
#4986=ORIENTED_EDGE ( 'NONE', *, *, #3806, .F. ) ;
#4989=DIRECTION ( 'NONE',  ( 1.000000000000000000, 0.000000000000000000, 0.000000000000000000 ) ) ;
#4990=VECTOR ( 'NONE', #3019, 1000.000000000000000 ) ;
#4997=DIRECTION ( 'NONE',  ( -3.903561672282191229E-16, 1.000000000000000000, 0.000000000000000000 ) ) ;
#5023=LINE ( 'NONE', #2091, #5338 ) ;
#5045=VECTOR ( 'NONE', #2566, 1000.000000000000000 ) ;
#5049=CIRCLE ( 'NONE', #2261, 72.49991987048069575 ) ;
#5060=DIRECTION ( 'NONE',  ( 0.000000000000000000, -0.000000000000000000, 1.000000000000000000 ) ) ;
#5070=EDGE_LOOP ( 'NONE', ( #1110, #2114, #1825, #4294 ) ) ;
#5081=EDGE_LOOP ( 'NONE', ( #5449, #4040, #4053, #317 ) ) ;
#5083=LINE ( 'NONE', #90, #5568 ) ;
#5089=DIRECTION ( 'NONE',  ( -1.000000000000000000, 0.000000000000000000, 0.000000000000000000 ) ) ;
#5091=VERTEX_POINT ( 'NONE', #2852 ) ;
#5092=DIRECTION ( 'NONE',  ( 0.000000000000000000, 0.000000000000000000, -1.000000000000000000 ) ) ;
#5102=AXIS2_PLACEMENT_3D ( 'NONE', #1484, #6321, #4898 ) ;
#5104=EDGE_CURVE ( 'NONE', #5616, #2301, #3175, .T. ) ;
#5110=VECTOR ( 'NONE', #6301, 1000.000000000000000 ) ;
#5112=CARTESIAN_POINT ( 'NONE',  ( 0.000000000000000000, 25.00000000000000000, 301.0000000000000568 ) ) ;
#5133=( GEOMETRIC_REPRESENTATION_CONTEXT ( 3 ) GLOBAL_UNCERTAINTY_ASSIGNED_CONTEXT ( ( #6117 ) ) GLOBAL_UNIT_ASSIGNED_CONTEXT ( ( #4863, #335, #4737 ) ) REPRESENTATION_CONTEXT ( 'NONE', 'WORKASPACE' ) );
#5152=ORIENTED_EDGE ( 'NONE', *, *, #2011, .F. ) ;
#5155=EDGE_CURVE ( 'NONE', #4162, #5856, #5685, .T. ) ;
#5165=DIRECTION ( 'NONE',  ( 0.000000000000000000, 1.000000000000000000, 0.000000000000000000 ) ) ;
#5185=DIRECTION ( 'NONE',  ( 1.000000000000000000, 0.000000000000000000, -0.000000000000000000 ) ) ;
#5198=VERTEX_POINT ( 'NONE', #2617 ) ;
#5214=CARTESIAN_POINT ( 'NONE',  ( 64.99991398172927859, 0.000000000000000000, 281.0000000000000000 ) ) ;
#5217=AXIS2_PLACEMENT_3D ( 'NONE', #3180, #5601, #6146 ) ;
#5245=ADVANCED_FACE ( 'NONE', ( #1138 ), #2168, .F. ) ;
#5250=EDGE_LOOP ( 'NONE', ( #2341, #1096, #3071, #6039 ) ) ;
#5252=ORIENTED_EDGE ( 'NONE', *, *, #1395, .F. ) ;
#5255=( LENGTH_UNIT ( ) NAMED_UNIT ( * ) SI_UNIT ( .MILLI., .METRE. ) );
#5273=ORIENTED_EDGE ( 'NONE', *, *, #1834, .T. ) ;
#5316=EDGE_CURVE ( 'NONE', #1997, #2301, #5818, .T. ) ;
#5338=VECTOR ( 'NONE', #622, 1000.000000000000000 ) ;
#5341=EDGE_CURVE ( 'NONE', #3812, #5742, #1887, .T. ) ;
#5343=CARTESIAN_POINT ( 'NONE',  ( 0.000000000000000000, 0.000000000000000000, 301.0000000000000568 ) ) ;
#5348=AXIS2_PLACEMENT_3D ( 'NONE', #4245, #847, #2800 ) ;
#5377=VERTEX_POINT ( 'NONE', #3266 ) ;
#5378=DIRECTION ( 'NONE',  ( -1.000000000000000000, 0.000000000000000000, 0.000000000000000000 ) ) ;
#5386=CARTESIAN_POINT ( 'NONE',  ( 0.000000000000000000, 76.99999716619419132, 276.0000000000000000 ) ) ;
#5389=DIRECTION ( 'NONE',  ( -0.000000000000000000, -0.000000000000000000, -1.000000000000000000 ) ) ;
#5407=DIRECTION ( 'NONE',  ( -1.000000000000000000, 0.000000000000000000, 0.000000000000000000 ) ) ;
#5423=DIRECTION ( 'NONE',  ( -1.000000000000000000, 0.000000000000000000, 0.000000000000000000 ) ) ;
#5436=ADVANCED_FACE ( 'NONE', ( #4812 ), #598, .F. ) ;
#5443=ADVANCED_FACE ( 'NONE', ( #1068 ), #1495, .F. ) ;
#5447=STYLED_ITEM('',(#6419),#4609);
#5449=ORIENTED_EDGE ( 'NONE', *, *, #4682, .F. ) ;
#5453=DIRECTION ( 'NONE',  ( -1.000000000000000000, -0.000000000000000000, -0.000000000000000000 ) ) ;
#5463=VECTOR ( 'NONE', #1509, 1000.000000000000000 ) ;
#5483=DIRECTION ( 'NONE',  ( 0.000000000000000000, 0.000000000000000000, 1.000000000000000000 ) ) ;
#5492=DIRECTION ( 'NONE',  ( 0.000000000000000000, 1.740526192617802767E-17, -1.000000000000000000 ) ) ;
#5493=FACE_OUTER_BOUND ( 'NONE', #4219, .T. ) ;
#5503=ORIENTED_EDGE ( 'NONE', *, *, #4201, .F. ) ;
#5505=EDGE_CURVE ( 'NONE', #5377, #2461, #1042, .T. ) ;
#5516=ORIENTED_EDGE ( 'NONE', *, *, #3736, .T. ) ;
#5520=AXIS2_PLACEMENT_3D ( 'NONE', #1150, #3117, #5060 ) ;
#5528=PRODUCT_DEFINITION_CONTEXT ( 'detailed design', #1178, 'design' ) ;
#5541=EDGE_CURVE ( 'NONE', #4432, #5958, #4026, .T. ) ;
#5562=AXIS2_PLACEMENT_3D ( 'NONE', #3566, #3113, #5089 ) ;
#5568=VECTOR ( 'NONE', #4464, 1000.000000000000000 ) ;
#5571=DIRECTION ( 'NONE',  ( 1.000000000000000000, 0.000000000000000000, 0.000000000000000000 ) ) ;
#5573=VECTOR ( 'NONE', #2150, 1000.000000000000000 ) ;
#5577=PLANE ( 'NONE',  #2985 ) ;
#5588=AXIS2_PLACEMENT_3D ( 'NONE', #4385, #5815, #1428 ) ;
#5595=CARTESIAN_POINT ( 'NONE',  ( 64.99991398172927859, 76.99999716619419132, 281.0000000000000000 ) ) ;
#5598=LINE ( 'NONE', #4015, #5045 ) ;
#5600=FACE_OUTER_BOUND ( 'NONE', #3039, .T. ) ;
#5601=DIRECTION ( 'NONE',  ( 0.000000000000000000, -1.740526192617802767E-17, -1.000000000000000000 ) ) ;
#5605=ORIENTED_EDGE ( 'NONE', *, *, #3074, .F. ) ;
#5616=VERTEX_POINT ( 'NONE', #3549 ) ;
#5619=DIRECTION ( 'NONE',  ( -0.000000000000000000, -0.000000000000000000, -1.000000000000000000 ) ) ;
#5630=PRODUCT_CONTEXT ( 'NONE', #4351, 'mechanical' ) ;
#5633=CYLINDRICAL_SURFACE ( 'NONE', #2158, 25.00000000000000000 ) ;
#5639=CARTESIAN_POINT ( 'NONE',  ( -3.081487911019577365E-30, 5.660601460262082306E-46, 281.0000000000000000 ) ) ;
#5640=AXIS2_PLACEMENT_3D ( 'NONE', #4839, #2386, #4346 ) ;
#5657=CARTESIAN_POINT ( 'NONE',  ( 0.000000000000000000, 0.000000000000000000, 281.0000000000000000 ) ) ;
#5678=VECTOR ( 'NONE', #3664, 1000.000000000000000 ) ;
#5685=LINE ( 'NONE', #2134, #99 ) ;
#5688=CARTESIAN_POINT ( 'NONE',  ( -3.081487911019577365E-30, 5.660601460262082306E-46, 0.000000000000000000 ) ) ;
#5704=ORIENTED_EDGE ( 'NONE', *, *, #3218, .F. ) ;
#5708=ORIENTED_EDGE ( 'NONE', *, *, #4564, .F. ) ;
#5719=CARTESIAN_POINT ( 'NONE',  ( 0.000000000000000000, 0.000000000000000000, 1.734723475976807094E-15 ) ) ;
#5726=CARTESIAN_POINT ( 'NONE',  ( 0.000000000000000000, 76.99999716619419132, 276.0000000000000000 ) ) ;
#5733=DIRECTION ( 'NONE',  ( -3.903561672282191229E-16, 1.000000000000000000, -0.000000000000000000 ) ) ;
#5742=VERTEX_POINT ( 'NONE', #402 ) ;
#5746=CARTESIAN_POINT ( 'NONE',  ( 3.122849337825746672E-15, 17.00000000000000000, 301.0000000000000568 ) ) ;
#5753=VERTEX_POINT ( 'NONE', #1384 ) ;
#5754=CIRCLE ( 'NONE', #4404, 17.00000000000000000 ) ;
#5756=EDGE_CURVE ( 'NONE', #258, #5742, #3050, .T. ) ;
#5763=ORIENTED_EDGE ( 'NONE', *, *, #5316, .T. ) ;
#5766=LINE ( 'NONE', #417, #5985 ) ;
#5770=CARTESIAN_POINT ( 'NONE',  ( -3.122849337825752983E-15, -17.00000000000000000, -20.00000000000000000 ) ) ;
#5772=CIRCLE ( 'NONE', #2053, 67.50000000000000000 ) ;
#5800=VERTEX_POINT ( 'NONE', #1035 ) ;
#5801=CARTESIAN_POINT ( 'NONE',  ( -1.331801922117356663E-14, -72.49991987048069575, 1.734723475976807094E-15 ) ) ;
#5804=FACE_OUTER_BOUND ( 'NONE', #1327, .T. ) ;
#5815=DIRECTION ( 'NONE',  ( 1.000000000000000000, -1.836970198721029194E-16, 0.000000000000000000 ) ) ;
#5817=EDGE_CURVE ( 'NONE', #2677, #1781, #67, .T. ) ;
#5818=LINE ( 'NONE', #6302, #1715 ) ;
#5839=EDGE_CURVE ( 'NONE', #2487, #6022, #4933, .T. ) ;
#5844=VECTOR ( 'NONE', #488, 1000.000000000000000 ) ;
#5856=VERTEX_POINT ( 'NONE', #2513 ) ;
#5859=AXIS2_PLACEMENT_3D ( 'NONE', #1544, #5389, #5935 ) ;
#5877=CARTESIAN_POINT ( 'NONE',  ( -4.592425496802576733E-15, -25.00000000000000000, 281.0000000000000000 ) ) ;
#5916=CARTESIAN_POINT ( 'NONE',  ( -3.081487911019577365E-30, 5.660601460262082306E-46, 0.000000000000000000 ) ) ;
#5934=AXIS2_PLACEMENT_3D ( 'NONE', #4089, #5492, #1073 ) ;
#5935=DIRECTION ( 'NONE',  ( -1.000000000000000000, 0.000000000000000000, 0.000000000000000000 ) ) ;
#5937=ADVANCED_FACE ( 'NONE', ( #231 ), #2120, .T. ) ;
#5938=ADVANCED_FACE ( 'NONE', ( #6061 ), #4532, .T. ) ;
#5944=PLANE ( 'NONE',  #2451 ) ;
#5945=EDGE_CURVE ( 'NONE', #2238, #1244, #3542, .T. ) ;
#5954=CARTESIAN_POINT ( 'NONE',  ( 64.99991398172927859, 76.99999716619419132, 281.0000000000000000 ) ) ;
#5957=CARTESIAN_POINT ( 'NONE',  ( 0.000000000000000000, 0.000000000000000000, -20.00000000000000000 ) ) ;
#5958=VERTEX_POINT ( 'NONE', #4138 ) ;
#5964=ORIENTED_EDGE ( 'NONE', *, *, #1834, .F. ) ;
#5985=VECTOR ( 'NONE', #3303, 1000.000000000000000 ) ;
#6021=CARTESIAN_POINT ( 'NONE',  ( 0.000000000000000000, 0.000000000000000000, -20.00000000000000000 ) ) ;
#6022=VERTEX_POINT ( 'NONE', #4020 ) ;
#6026=EDGE_CURVE ( 'NONE', #3408, #5800, #5023, .T. ) ;
#6039=ORIENTED_EDGE ( 'NONE', *, *, #5341, .F. ) ;
#6040=AXIS2_PLACEMENT_3D ( 'NONE', #5719, #5619, #4713 ) ;
#6053=ORIENTED_EDGE ( 'NONE', *, *, #5505, .T. ) ;
#6061=FACE_OUTER_BOUND ( 'NONE', #3160, .T. ) ;
#6079=VECTOR ( 'NONE', #3276, 1000.000000000000000 ) ;
#6084=ORIENTED_EDGE ( 'NONE', *, *, #1048, .T. ) ;
#6089=ADVANCED_FACE ( 'NONE', ( #5804 ), #4171, .T. ) ;
#6114=DIRECTION ( 'NONE',  ( -0.000000000000000000, -0.000000000000000000, 1.000000000000000000 ) ) ;
#6117=UNCERTAINTY_MEASURE_WITH_UNIT (LENGTH_MEASURE( 1.000000000000000082E-05 ), #4863, 'distance_accuracy_value', 'NONE');
#6144=AXIS2_PLACEMENT_3D ( 'NONE', #2425, #17, #3456 ) ;
#6146=DIRECTION ( 'NONE',  ( 0.000000000000000000, 1.000000000000000000, 0.000000000000000000 ) ) ;
#6166=AXIS2_PLACEMENT_3D ( 'NONE', #3648, #667, #182 ) ;
#6167=PRODUCT_DEFINITION_SHAPE ( 'NONE', 'NONE',  #2008 ) ;
#6170=CARTESIAN_POINT ( 'NONE',  ( 59.99991398172927859, 76.99999716619419132, 5.000000000000000000 ) ) ;
#6176=ORIENTED_EDGE ( 'NONE', *, *, #4768, .F. ) ;
#6221=CARTESIAN_POINT ( 'NONE',  ( -1.331801922117356663E-14, -72.49991987048069575, 281.0000000000000000 ) ) ;
#6236=DIRECTION ( 'NONE',  ( -0.000000000000000000, -0.000000000000000000, 1.000000000000000000 ) ) ;
#6239=VECTOR ( 'NONE', #2655, 1000.000000000000000 ) ;
#6262=ORIENTED_EDGE ( 'NONE', *, *, #5104, .T. ) ;
#6264=VERTEX_POINT ( 'NONE', #2890 ) ;
#6272=ORIENTED_EDGE ( 'NONE', *, *, #5839, .T. ) ;
#6301=DIRECTION ( 'NONE',  ( -3.903561672282183340E-16, 1.000000000000000000, -0.000000000000000000 ) ) ;
#6302=CARTESIAN_POINT ( 'NONE',  ( 0.000000000000000000, 76.99999716619419132, 5.000000000000000000 ) ) ;
#6313=ORIENTED_EDGE ( 'NONE', *, *, #1732, .F. ) ;
#6320=DIRECTION ( 'NONE',  ( -3.903561672282183340E-16, 1.000000000000000000, 0.000000000000000000 ) ) ;
#6321=DIRECTION ( 'NONE',  ( 0.000000000000000000, 0.000000000000000000, 1.000000000000000000 ) ) ;
#6324=VERTEX_POINT ( 'NONE', #5386 ) ;
#6349=AXIS2_PLACEMENT_3D ( 'NONE', #290, #2242, #4169 ) ;
#6358=EDGE_CURVE ( 'NONE', #5091, #5198, #969, .T. ) ;
#6413=COLOUR_RGB('Off White',0.89,0.88,0.83);
#6414=FILL_AREA_STYLE_COLOUR('',#6413);
#6415=FILL_AREA_STYLE('',(#6414));
#6416=SURFACE_STYLE_FILL_AREA(#6415);
#6417=SURFACE_SIDE_STYLE('',(#6416));
#6418=SURFACE_STYLE_USAGE(.BOTH.,#6417);
#6419=PRESENTATION_STYLE_ASSIGNMENT((#6418));
ENDSEC;
END-ISO-10303-21;
